ISO-10303-21;
HEADER;
/* Generated by software containing ST-Developer
 * from STEP Tools, Inc. (www.steptools.com) 
 */

FILE_DESCRIPTION(
/* description */ ('Bearing-mounted hook block'),
/* implementation_level */ '2;1');

FILE_NAME(
/* name */ 'Hex Nut - M8.step',
/* time_stamp */ '2026-10-28T22:30:11-07:00',
/* author */ (''),
/* organization */ (''),
/* preprocessor_version */ 'ST-DEVELOPER v20.2',
/* originating_system */ 'Autodesk Translation Framework v15.17.0.0',
/* authorisation */ '');

FILE_SCHEMA (('AUTOMOTIVE_DESIGN { 1 0 10303 214 3 1 1 }'));
ENDSEC;

DATA;
#10=MECHANICAL_DESIGN_GEOMETRIC_PRESENTATION_REPRESENTATION('',(#333),#7609);
#239=(
BOUNDED_CURVE()
B_SPLINE_CURVE(2,(#6451,#6452,#6453),.UNSPECIFIED.,.F.,.F.)
B_SPLINE_CURVE_WITH_KNOTS((3,3),(0.14973948338295,0.97160236658079),
 .UNSPECIFIED.)
CURVE()
GEOMETRIC_REPRESENTATION_ITEM()
RATIONAL_B_SPLINE_CURVE((1.07140024848292,1.23714644374248,1.07140024848292))
REPRESENTATION_ITEM('')
);
#240=(
BOUNDED_CURVE()
B_SPLINE_CURVE(2,(#6455,#6456,#6457),.UNSPECIFIED.,.F.,.F.)
B_SPLINE_CURVE_WITH_KNOTS((3,3),(0.14973948338295,0.971602366580789),
 .UNSPECIFIED.)
CURVE()
GEOMETRIC_REPRESENTATION_ITEM()
RATIONAL_B_SPLINE_CURVE((1.07140024848292,1.23714644374248,1.07140024848292))
REPRESENTATION_ITEM('')
);
#241=(
BOUNDED_CURVE()
B_SPLINE_CURVE(2,(#6462,#6463,#6464),.UNSPECIFIED.,.F.,.F.)
B_SPLINE_CURVE_WITH_KNOTS((3,3),(0.14973948338295,0.97160236658079),
 .UNSPECIFIED.)
CURVE()
GEOMETRIC_REPRESENTATION_ITEM()
RATIONAL_B_SPLINE_CURVE((1.07140024848292,1.23714644374248,1.07140024848292))
REPRESENTATION_ITEM('')
);
#242=(
BOUNDED_CURVE()
B_SPLINE_CURVE(2,(#6466,#6467,#6468),.UNSPECIFIED.,.F.,.F.)
B_SPLINE_CURVE_WITH_KNOTS((3,3),(0.14973948338295,0.97160236658079),
 .UNSPECIFIED.)
CURVE()
GEOMETRIC_REPRESENTATION_ITEM()
RATIONAL_B_SPLINE_CURVE((1.07140024848292,1.23714644374248,1.07140024848292))
REPRESENTATION_ITEM('')
);
#243=(
BOUNDED_CURVE()
B_SPLINE_CURVE(2,(#6470,#6471,#6472),.UNSPECIFIED.,.F.,.F.)
B_SPLINE_CURVE_WITH_KNOTS((3,3),(0.14973948338295,0.971602366580789),
 .UNSPECIFIED.)
CURVE()
GEOMETRIC_REPRESENTATION_ITEM()
RATIONAL_B_SPLINE_CURVE((1.07140024848292,1.23714644374248,1.07140024848292))
REPRESENTATION_ITEM('')
);
#244=(
BOUNDED_CURVE()
B_SPLINE_CURVE(2,(#6473,#6474,#6475),.UNSPECIFIED.,.F.,.F.)
B_SPLINE_CURVE_WITH_KNOTS((3,3),(0.14973948338295,0.97160236658079),
 .UNSPECIFIED.)
CURVE()
GEOMETRIC_REPRESENTATION_ITEM()
RATIONAL_B_SPLINE_CURVE((1.07140024848292,1.23714644374248,1.07140024848292))
REPRESENTATION_ITEM('')
);
#245=(
BOUNDED_CURVE()
B_SPLINE_CURVE(2,(#6482,#6483,#6484),.UNSPECIFIED.,.F.,.F.)
B_SPLINE_CURVE_WITH_KNOTS((3,3),(0.14973948338295,0.97160236658079),
 .UNSPECIFIED.)
CURVE()
GEOMETRIC_REPRESENTATION_ITEM()
RATIONAL_B_SPLINE_CURVE((1.07140024848292,1.23714644374248,1.07140024848292))
REPRESENTATION_ITEM('')
);
#246=(
BOUNDED_CURVE()
B_SPLINE_CURVE(2,(#6486,#6487,#6488),.UNSPECIFIED.,.F.,.F.)
B_SPLINE_CURVE_WITH_KNOTS((3,3),(0.14973948338295,0.97160236658079),
 .UNSPECIFIED.)
CURVE()
GEOMETRIC_REPRESENTATION_ITEM()
RATIONAL_B_SPLINE_CURVE((1.07140024848292,1.23714644374248,1.07140024848292))
REPRESENTATION_ITEM('')
);
#247=(
BOUNDED_CURVE()
B_SPLINE_CURVE(2,(#6490,#6491,#6492),.UNSPECIFIED.,.F.,.F.)
B_SPLINE_CURVE_WITH_KNOTS((3,3),(0.14973948338295,0.971602366580789),
 .UNSPECIFIED.)
CURVE()
GEOMETRIC_REPRESENTATION_ITEM()
RATIONAL_B_SPLINE_CURVE((1.07140024848292,1.23714644374248,1.07140024848292))
REPRESENTATION_ITEM('')
);
#248=(
BOUNDED_CURVE()
B_SPLINE_CURVE(2,(#6494,#6495,#6496),.UNSPECIFIED.,.F.,.F.)
B_SPLINE_CURVE_WITH_KNOTS((3,3),(0.14973948338295,0.97160236658079),
 .UNSPECIFIED.)
CURVE()
GEOMETRIC_REPRESENTATION_ITEM()
RATIONAL_B_SPLINE_CURVE((1.07140024848292,1.23714644374248,1.07140024848292))
REPRESENTATION_ITEM('')
);
#249=(
BOUNDED_CURVE()
B_SPLINE_CURVE(2,(#6498,#6499,#6500),.UNSPECIFIED.,.F.,.F.)
B_SPLINE_CURVE_WITH_KNOTS((3,3),(0.14973948338295,0.97160236658079),
 .UNSPECIFIED.)
CURVE()
GEOMETRIC_REPRESENTATION_ITEM()
RATIONAL_B_SPLINE_CURVE((1.07140024848292,1.23714644374248,1.07140024848292))
REPRESENTATION_ITEM('')
);
#250=(
BOUNDED_CURVE()
B_SPLINE_CURVE(2,(#6501,#6502,#6503),.UNSPECIFIED.,.F.,.F.)
B_SPLINE_CURVE_WITH_KNOTS((3,3),(0.14973948338295,0.971602366580789),
 .UNSPECIFIED.)
CURVE()
GEOMETRIC_REPRESENTATION_ITEM()
RATIONAL_B_SPLINE_CURVE((1.07140024848292,1.23714644374248,1.07140024848292))
REPRESENTATION_ITEM('')
);
#254=CONICAL_SURFACE('',#4394,0.734027674973257,1.0471975511966);
#255=CONICAL_SURFACE('',#4396,0.734027674973257,1.0471975511966);
#285=SHAPE_REPRESENTATION_RELATIONSHIP('SRR','None',#7732,#309);
#309=ADVANCED_BREP_SHAPE_REPRESENTATION('',(#364),#7592);
#333=STYLED_ITEM('',(#7938),#364);
#364=MANIFOLD_SOLID_BREP('Body1',#3930);
#479=LINE('',#6459,#709);
#480=LINE('',#6480,#710);
#481=LINE('',#6505,#711);
#482=LINE('',#6506,#712);
#483=LINE('',#6508,#713);
#484=LINE('',#6510,#714);
#485=LINE('',#6515,#715);
#486=LINE('',#6518,#716);
#487=LINE('',#6520,#717);
#709=VECTOR('',#5204,0.734027674973257);
#710=VECTOR('',#5211,0.734027674973257);
#711=VECTOR('',#5214,1.);
#712=VECTOR('',#5215,1.);
#713=VECTOR('',#5218,1.);
#714=VECTOR('',#5221,1.);
#715=VECTOR('',#5226,0.4);
#716=VECTOR('',#5231,1.);
#717=VECTOR('',#5234,1.);
#878=CYLINDRICAL_SURFACE('',#4401,0.338975);
#957=FACE_BOUND('',#1366,.T.);
#958=FACE_BOUND('',#1368,.T.);
#1084=FACE_OUTER_BOUND('',#1356,.T.);
#1085=FACE_OUTER_BOUND('',#1357,.T.);
#1086=FACE_OUTER_BOUND('',#1358,.T.);
#1087=FACE_OUTER_BOUND('',#1359,.T.);
#1088=FACE_OUTER_BOUND('',#1360,.T.);
#1089=FACE_OUTER_BOUND('',#1361,.T.);
#1090=FACE_OUTER_BOUND('',#1362,.T.);
#1091=FACE_OUTER_BOUND('',#1363,.T.);
#1092=FACE_OUTER_BOUND('',#1364,.T.);
#1093=FACE_OUTER_BOUND('',#1365,.T.);
#1094=FACE_OUTER_BOUND('',#1367,.T.);
#1356=EDGE_LOOP('',(#2938,#2939,#2940,#2941,#2942,#2943,#2944,#2945,#2946));
#1357=EDGE_LOOP('',(#2947,#2948,#2949,#2950,#2951,#2952,#2953,#2954,#2955));
#1358=EDGE_LOOP('',(#2956,#2957,#2958,#2959));
#1359=EDGE_LOOP('',(#2960,#2961,#2962,#2963));
#1360=EDGE_LOOP('',(#2964,#2965,#2966,#2967));
#1361=EDGE_LOOP('',(#2968,#2969,#2970,#2971));
#1362=EDGE_LOOP('',(#2972,#2973,#2974,#2975));
#1363=EDGE_LOOP('',(#2976,#2977,#2978,#2979));
#1364=EDGE_LOOP('',(#2980,#2981,#2982,#2983));
#1365=EDGE_LOOP('',(#2984));
#1366=EDGE_LOOP('',(#2985));
#1367=EDGE_LOOP('',(#2986));
#1368=EDGE_LOOP('',(#2987));
#1632=CIRCLE('',#4395,0.6175);
#1633=CIRCLE('',#4397,0.6175);
#1634=CIRCLE('',#4402,0.338975);
#1635=CIRCLE('',#4403,0.338975);
#1893=VERTEX_POINT('',#6449);
#1894=VERTEX_POINT('',#6450);
#1895=VERTEX_POINT('',#6454);
#1896=VERTEX_POINT('',#6458);
#1897=VERTEX_POINT('',#6461);
#1898=VERTEX_POINT('',#6465);
#1899=VERTEX_POINT('',#6469);
#1900=VERTEX_POINT('',#6477);
#1901=VERTEX_POINT('',#6479);
#1902=VERTEX_POINT('',#6481);
#1903=VERTEX_POINT('',#6485);
#1904=VERTEX_POINT('',#6489);
#1905=VERTEX_POINT('',#6493);
#1906=VERTEX_POINT('',#6497);
#1907=VERTEX_POINT('',#6512);
#1908=VERTEX_POINT('',#6514);
#2279=EDGE_CURVE('',#1893,#1894,#239,.T.);
#2280=EDGE_CURVE('',#1895,#1893,#240,.T.);
#2281=EDGE_CURVE('',#1895,#1896,#479,.T.);
#2282=EDGE_CURVE('',#1896,#1896,#1632,.T.);
#2283=EDGE_CURVE('',#1897,#1895,#241,.T.);
#2284=EDGE_CURVE('',#1898,#1897,#242,.T.);
#2285=EDGE_CURVE('',#1899,#1898,#243,.T.);
#2286=EDGE_CURVE('',#1894,#1899,#244,.T.);
#2287=EDGE_CURVE('',#1900,#1900,#1633,.T.);
#2288=EDGE_CURVE('',#1900,#1901,#480,.T.);
#2289=EDGE_CURVE('',#1902,#1901,#245,.T.);
#2290=EDGE_CURVE('',#1903,#1902,#246,.T.);
#2291=EDGE_CURVE('',#1904,#1903,#247,.T.);
#2292=EDGE_CURVE('',#1905,#1904,#248,.T.);
#2293=EDGE_CURVE('',#1906,#1905,#249,.T.);
#2294=EDGE_CURVE('',#1901,#1906,#250,.T.);
#2295=EDGE_CURVE('',#1897,#1906,#481,.T.);
#2296=EDGE_CURVE('',#1898,#1905,#482,.T.);
#2297=EDGE_CURVE('',#1895,#1901,#483,.T.);
#2298=EDGE_CURVE('',#1893,#1902,#484,.T.);
#2299=EDGE_CURVE('',#1907,#1907,#1634,.F.);
#2300=EDGE_CURVE('',#1907,#1908,#485,.T.);
#2301=EDGE_CURVE('',#1908,#1908,#1635,.F.);
#2302=EDGE_CURVE('',#1894,#1903,#486,.T.);
#2303=EDGE_CURVE('',#1899,#1904,#487,.T.);
#2938=ORIENTED_EDGE('',*,*,#2279,.F.);
#2939=ORIENTED_EDGE('',*,*,#2280,.F.);
#2940=ORIENTED_EDGE('',*,*,#2281,.T.);
#2941=ORIENTED_EDGE('',*,*,#2282,.F.);
#2942=ORIENTED_EDGE('',*,*,#2281,.F.);
#2943=ORIENTED_EDGE('',*,*,#2283,.F.);
#2944=ORIENTED_EDGE('',*,*,#2284,.F.);
#2945=ORIENTED_EDGE('',*,*,#2285,.F.);
#2946=ORIENTED_EDGE('',*,*,#2286,.F.);
#2947=ORIENTED_EDGE('',*,*,#2287,.F.);
#2948=ORIENTED_EDGE('',*,*,#2288,.T.);
#2949=ORIENTED_EDGE('',*,*,#2289,.F.);
#2950=ORIENTED_EDGE('',*,*,#2290,.F.);
#2951=ORIENTED_EDGE('',*,*,#2291,.F.);
#2952=ORIENTED_EDGE('',*,*,#2292,.F.);
#2953=ORIENTED_EDGE('',*,*,#2293,.F.);
#2954=ORIENTED_EDGE('',*,*,#2294,.F.);
#2955=ORIENTED_EDGE('',*,*,#2288,.F.);
#2956=ORIENTED_EDGE('',*,*,#2284,.T.);
#2957=ORIENTED_EDGE('',*,*,#2295,.T.);
#2958=ORIENTED_EDGE('',*,*,#2293,.T.);
#2959=ORIENTED_EDGE('',*,*,#2296,.F.);
#2960=ORIENTED_EDGE('',*,*,#2283,.T.);
#2961=ORIENTED_EDGE('',*,*,#2297,.T.);
#2962=ORIENTED_EDGE('',*,*,#2294,.T.);
#2963=ORIENTED_EDGE('',*,*,#2295,.F.);
#2964=ORIENTED_EDGE('',*,*,#2280,.T.);
#2965=ORIENTED_EDGE('',*,*,#2298,.T.);
#2966=ORIENTED_EDGE('',*,*,#2289,.T.);
#2967=ORIENTED_EDGE('',*,*,#2297,.F.);
#2968=ORIENTED_EDGE('',*,*,#2299,.F.);
#2969=ORIENTED_EDGE('',*,*,#2300,.T.);
#2970=ORIENTED_EDGE('',*,*,#2301,.T.);
#2971=ORIENTED_EDGE('',*,*,#2300,.F.);
#2972=ORIENTED_EDGE('',*,*,#2279,.T.);
#2973=ORIENTED_EDGE('',*,*,#2302,.T.);
#2974=ORIENTED_EDGE('',*,*,#2290,.T.);
#2975=ORIENTED_EDGE('',*,*,#2298,.F.);
#2976=ORIENTED_EDGE('',*,*,#2285,.T.);
#2977=ORIENTED_EDGE('',*,*,#2296,.T.);
#2978=ORIENTED_EDGE('',*,*,#2292,.T.);
#2979=ORIENTED_EDGE('',*,*,#2303,.F.);
#2980=ORIENTED_EDGE('',*,*,#2286,.T.);
#2981=ORIENTED_EDGE('',*,*,#2303,.T.);
#2982=ORIENTED_EDGE('',*,*,#2291,.T.);
#2983=ORIENTED_EDGE('',*,*,#2302,.F.);
#2984=ORIENTED_EDGE('',*,*,#2287,.T.);
#2985=ORIENTED_EDGE('',*,*,#2299,.T.);
#2986=ORIENTED_EDGE('',*,*,#2282,.T.);
#2987=ORIENTED_EDGE('',*,*,#2301,.F.);
#3606=PLANE('',#4398);
#3607=PLANE('',#4399);
#3608=PLANE('',#4400);
#3609=PLANE('',#4404);
#3610=PLANE('',#4405);
#3611=PLANE('',#4406);
#3612=PLANE('',#4407);
#3613=PLANE('',#4408);
#3766=ADVANCED_FACE('',(#1084),#254,.T.);
#3767=ADVANCED_FACE('',(#1085),#255,.T.);
#3768=ADVANCED_FACE('',(#1086),#3606,.T.);
#3769=ADVANCED_FACE('',(#1087),#3607,.T.);
#3770=ADVANCED_FACE('',(#1088),#3608,.T.);
#3771=ADVANCED_FACE('',(#1089),#878,.F.);
#3772=ADVANCED_FACE('',(#1090),#3609,.T.);
#3773=ADVANCED_FACE('',(#1091),#3610,.T.);
#3774=ADVANCED_FACE('',(#1092),#3611,.T.);
#3775=ADVANCED_FACE('',(#1093,#957),#3612,.T.);
#3776=ADVANCED_FACE('',(#1094,#958),#3613,.F.);
#3930=CLOSED_SHELL('',(#3766,#3767,#3768,#3769,#3770,#3771,#3772,#3773,
#3774,#3775,#3776));
#4393=AXIS2_PLACEMENT_3D('',#6447,#5200,#5201);
#4394=AXIS2_PLACEMENT_3D('',#6448,#5202,#5203);
#4395=AXIS2_PLACEMENT_3D('',#6460,#5205,#5206);
#4396=AXIS2_PLACEMENT_3D('',#6476,#5207,#5208);
#4397=AXIS2_PLACEMENT_3D('',#6478,#5209,#5210);
#4398=AXIS2_PLACEMENT_3D('',#6504,#5212,#5213);
#4399=AXIS2_PLACEMENT_3D('',#6507,#5216,#5217);
#4400=AXIS2_PLACEMENT_3D('',#6509,#5219,#5220);
#4401=AXIS2_PLACEMENT_3D('',#6511,#5222,#5223);
#4402=AXIS2_PLACEMENT_3D('',#6513,#5224,#5225);
#4403=AXIS2_PLACEMENT_3D('',#6516,#5227,#5228);
#4404=AXIS2_PLACEMENT_3D('',#6517,#5229,#5230);
#4405=AXIS2_PLACEMENT_3D('',#6519,#5232,#5233);
#4406=AXIS2_PLACEMENT_3D('',#6521,#5235,#5236);
#4407=AXIS2_PLACEMENT_3D('',#6522,#5237,#5238);
#4408=AXIS2_PLACEMENT_3D('',#6523,#5239,#5240);
#5200=DIRECTION('axis',(0.,0.,1.));
#5201=DIRECTION('refdir',(1.,0.,0.));
#5202=DIRECTION('center_axis',(0.,1.,0.));
#5203=DIRECTION('ref_axis',(1.,0.,0.));
#5204=DIRECTION('',(0.866025403784439,-0.5,1.06057523872491E-16));
#5205=DIRECTION('center_axis',(0.,-1.,0.));
#5206=DIRECTION('ref_axis',(1.,0.,0.));
#5207=DIRECTION('center_axis',(0.,-1.,0.));
#5208=DIRECTION('ref_axis',(1.,0.,0.));
#5209=DIRECTION('center_axis',(0.,1.,0.));
#5210=DIRECTION('ref_axis',(1.,0.,0.));
#5211=DIRECTION('',(-0.866025403784439,-0.5,-1.06057523872491E-16));
#5212=DIRECTION('center_axis',(1.4792020664489E-16,0.,-1.));
#5213=DIRECTION('ref_axis',(-1.,0.,-1.4792020664489E-16));
#5214=DIRECTION('',(0.,1.,0.));
#5215=DIRECTION('',(0.,1.,0.));
#5216=DIRECTION('center_axis',(-0.866025403784439,0.,-0.5));
#5217=DIRECTION('ref_axis',(-0.5,0.,0.866025403784439));
#5218=DIRECTION('',(0.,1.,0.));
#5219=DIRECTION('center_axis',(-0.866025403784439,0.,0.5));
#5220=DIRECTION('ref_axis',(0.5,0.,0.866025403784439));
#5221=DIRECTION('',(0.,1.,0.));
#5222=DIRECTION('center_axis',(0.,1.,0.));
#5223=DIRECTION('ref_axis',(1.,0.,0.));
#5224=DIRECTION('center_axis',(0.,1.,0.));
#5225=DIRECTION('ref_axis',(1.,0.,0.));
#5226=DIRECTION('',(0.,-1.,0.));
#5227=DIRECTION('center_axis',(0.,1.,0.));
#5228=DIRECTION('ref_axis',(1.,0.,0.));
#5229=DIRECTION('center_axis',(-2.95840413289779E-16,0.,1.));
#5230=DIRECTION('ref_axis',(1.,0.,2.95840413289779E-16));
#5231=DIRECTION('',(0.,1.,0.));
#5232=DIRECTION('center_axis',(0.866025403784439,0.,-0.5));
#5233=DIRECTION('ref_axis',(-0.5,0.,-0.866025403784439));
#5234=DIRECTION('',(0.,1.,0.));
#5235=DIRECTION('center_axis',(0.866025403784439,0.,0.5));
#5236=DIRECTION('ref_axis',(0.5,0.,-0.866025403784439));
#5237=DIRECTION('center_axis',(0.,1.,0.));
#5238=DIRECTION('ref_axis',(1.,0.,0.));
#5239=DIRECTION('center_axis',(0.,1.,0.));
#5240=DIRECTION('ref_axis',(1.,0.,0.));
#6447=CARTESIAN_POINT('',(0.,0.,0.));
#6448=CARTESIAN_POINT('Origin',(0.,0.067277284513851,0.));
#6449=CARTESIAN_POINT('',(-0.375277674973257,0.0768195421087395,0.65));
#6450=CARTESIAN_POINT('',(0.375277674973257,0.0768195421087395,0.65));
#6451=CARTESIAN_POINT('Ctrl Pts',(-0.375277674973257,0.0768195421087395,
0.65));
#6452=CARTESIAN_POINT('Ctrl Pts',(1.66533453693773E-13,-0.0315137912242439,
0.65));
#6453=CARTESIAN_POINT('Ctrl Pts',(0.375277674973257,0.0768195421087394,
0.65));
#6454=CARTESIAN_POINT('',(-0.750555349946514,0.0768195421087394,-9.19165206894919E-17));
#6455=CARTESIAN_POINT('Ctrl Pts',(-0.750555349946514,0.0768195421087394,
-9.19165206894919E-17));
#6456=CARTESIAN_POINT('Ctrl Pts',(-0.562916512459802,-0.0315137912242434,
0.325000000000144));
#6457=CARTESIAN_POINT('Ctrl Pts',(-0.375277674973257,0.0768195421087395,
0.65));
#6458=CARTESIAN_POINT('',(-0.6175,-2.77555756156289E-17,-7.5621939847349E-17));
#6459=CARTESIAN_POINT('',(-0.734027674973257,0.067277284513851,-8.98924642641573E-17));
#6460=CARTESIAN_POINT('Origin',(0.,0.,0.));
#6461=CARTESIAN_POINT('',(-0.375277674973257,0.0768195421087395,-0.65));
#6462=CARTESIAN_POINT('Ctrl Pts',(-0.375277674973257,0.0768195421087395,
-0.65));
#6463=CARTESIAN_POINT('Ctrl Pts',(-0.562916512459968,-0.0315137912242437,
-0.324999999999856));
#6464=CARTESIAN_POINT('Ctrl Pts',(-0.750555349946514,0.0768195421087395,
-9.19165206894919E-17));
#6465=CARTESIAN_POINT('',(0.375277674973257,0.0768195421087395,-0.65));
#6466=CARTESIAN_POINT('Ctrl Pts',(0.375277674973257,0.0768195421087395,
-0.65));
#6467=CARTESIAN_POINT('Ctrl Pts',(-1.66144875635155E-13,-0.0315137912242437,
-0.65));
#6468=CARTESIAN_POINT('Ctrl Pts',(-0.375277674973257,0.0768195421087395,
-0.65));
#6469=CARTESIAN_POINT('',(0.750555349946514,0.0768195421087394,0.));
#6470=CARTESIAN_POINT('Ctrl Pts',(0.750555349946514,0.0768195421087394,
0.));
#6471=CARTESIAN_POINT('Ctrl Pts',(0.562916512459802,-0.0315137912242436,
-0.325000000000144));
#6472=CARTESIAN_POINT('Ctrl Pts',(0.375277674973257,0.0768195421087395,
-0.65));
#6473=CARTESIAN_POINT('Ctrl Pts',(0.375277674973257,0.0768195421087394,
0.65));
#6474=CARTESIAN_POINT('Ctrl Pts',(0.562916512459968,-0.0315137912242439,
0.324999999999856));
#6475=CARTESIAN_POINT('Ctrl Pts',(0.750555349946514,0.0768195421087394,
0.));
#6476=CARTESIAN_POINT('Origin',(0.,0.612722715486149,0.));
#6477=CARTESIAN_POINT('',(-0.6175,0.68,-7.5621939847349E-17));
#6478=CARTESIAN_POINT('Origin',(0.,0.68,0.));
#6479=CARTESIAN_POINT('',(-0.750555349946514,0.603180457891261,-9.19165206894919E-17));
#6480=CARTESIAN_POINT('',(-0.734027674973257,0.612722715486149,-8.98924642641573E-17));
#6481=CARTESIAN_POINT('',(-0.375277674973257,0.603180457891261,0.65));
#6482=CARTESIAN_POINT('Ctrl Pts',(-0.375277674973257,0.603180457891261,
0.65));
#6483=CARTESIAN_POINT('Ctrl Pts',(-0.562916512459968,0.711513791224243,
0.324999999999856));
#6484=CARTESIAN_POINT('Ctrl Pts',(-0.750555349946514,0.603180457891261,
-9.19165206894919E-17));
#6485=CARTESIAN_POINT('',(0.375277674973257,0.603180457891261,0.65));
#6486=CARTESIAN_POINT('Ctrl Pts',(0.375277674973257,0.603180457891261,0.65));
#6487=CARTESIAN_POINT('Ctrl Pts',(-1.66755498298699E-13,0.711513791224244,
0.65));
#6488=CARTESIAN_POINT('Ctrl Pts',(-0.375277674973257,0.603180457891261,
0.65));
#6489=CARTESIAN_POINT('',(0.750555349946514,0.603180457891261,0.));
#6490=CARTESIAN_POINT('Ctrl Pts',(0.750555349946514,0.603180457891261,0.));
#6491=CARTESIAN_POINT('Ctrl Pts',(0.562916512459802,0.711513791224244,0.325000000000144));
#6492=CARTESIAN_POINT('Ctrl Pts',(0.375277674973257,0.603180457891261,0.65));
#6493=CARTESIAN_POINT('',(0.375277674973257,0.603180457891261,-0.65));
#6494=CARTESIAN_POINT('Ctrl Pts',(0.375277674973257,0.603180457891261,-0.65));
#6495=CARTESIAN_POINT('Ctrl Pts',(0.562916512459969,0.711513791224244,-0.324999999999856));
#6496=CARTESIAN_POINT('Ctrl Pts',(0.750555349946514,0.603180457891261,0.));
#6497=CARTESIAN_POINT('',(-0.375277674973257,0.603180457891261,-0.65));
#6498=CARTESIAN_POINT('Ctrl Pts',(-0.375277674973257,0.603180457891261,
-0.65));
#6499=CARTESIAN_POINT('Ctrl Pts',(1.66422431391311E-13,0.711513791224244,
-0.65));
#6500=CARTESIAN_POINT('Ctrl Pts',(0.375277674973257,0.603180457891261,-0.65));
#6501=CARTESIAN_POINT('Ctrl Pts',(-0.750555349946514,0.603180457891261,
-9.19165206894919E-17));
#6502=CARTESIAN_POINT('Ctrl Pts',(-0.562916512459802,0.711513791224244,
-0.325000000000144));
#6503=CARTESIAN_POINT('Ctrl Pts',(-0.375277674973257,0.603180457891261,
-0.65));
#6504=CARTESIAN_POINT('Origin',(0.375277674973257,0.,-0.65));
#6505=CARTESIAN_POINT('',(-0.375277674973257,0.,-0.65));
#6506=CARTESIAN_POINT('',(0.375277674973257,0.,-0.65));
#6507=CARTESIAN_POINT('Origin',(-0.375277674973257,0.,-0.65));
#6508=CARTESIAN_POINT('',(-0.750555349946514,0.,-9.19165206894919E-17));
#6509=CARTESIAN_POINT('Origin',(-0.750555349946514,0.,-9.19165206894919E-17));
#6510=CARTESIAN_POINT('',(-0.375277674973257,0.,0.65));
#6511=CARTESIAN_POINT('Origin',(0.,0.,0.));
#6512=CARTESIAN_POINT('',(-0.338975,0.68,4.15124648740974E-17));
#6513=CARTESIAN_POINT('Origin',(0.,0.68,0.));
#6514=CARTESIAN_POINT('',(-0.338975,0.,4.15124648740974E-17));
#6515=CARTESIAN_POINT('',(-0.338975,0.,4.15124648740974E-17));
#6516=CARTESIAN_POINT('Origin',(0.,0.,0.));
#6517=CARTESIAN_POINT('Origin',(-0.375277674973257,0.,0.65));
#6518=CARTESIAN_POINT('',(0.375277674973257,0.,0.65));
#6519=CARTESIAN_POINT('Origin',(0.750555349946514,0.,0.));
#6520=CARTESIAN_POINT('',(0.750555349946514,0.,0.));
#6521=CARTESIAN_POINT('Origin',(0.375277674973257,0.,0.65));
#6522=CARTESIAN_POINT('Origin',(0.,0.68,-1.11022302462516E-16));
#6523=CARTESIAN_POINT('Origin',(0.,0.,-1.11022302462516E-16));
#7562=UNCERTAINTY_MEASURE_WITH_UNIT(LENGTH_MEASURE(0.001),#7610,
'DISTANCE_ACCURACY_VALUE',
'Maximum model space distance between geometric entities at asserted c
onnectivities');
#7579=UNCERTAINTY_MEASURE_WITH_UNIT(LENGTH_MEASURE(0.001),#7610,
'DISTANCE_ACCURACY_VALUE',
'Maximum model space distance between geometric entities at asserted c
onnectivities');
#7592=(
GEOMETRIC_REPRESENTATION_CONTEXT(3)
GLOBAL_UNCERTAINTY_ASSIGNED_CONTEXT((#7562))
GLOBAL_UNIT_ASSIGNED_CONTEXT((#7610,#7612,#7613))
REPRESENTATION_CONTEXT('','3D')
);
#7609=(
GEOMETRIC_REPRESENTATION_CONTEXT(3)
GLOBAL_UNCERTAINTY_ASSIGNED_CONTEXT((#7579))
GLOBAL_UNIT_ASSIGNED_CONTEXT((#7610,#7612,#7613))
REPRESENTATION_CONTEXT('','3D')
);
#7610=(
LENGTH_UNIT()
NAMED_UNIT(*)
SI_UNIT(.CENTI.,.METRE.)
);
#7612=(
NAMED_UNIT(*)
PLANE_ANGLE_UNIT()
SI_UNIT($,.RADIAN.)
);
#7613=(
NAMED_UNIT(*)
SI_UNIT($,.STERADIAN.)
SOLID_ANGLE_UNIT()
);
#7626=SHAPE_DEFINITION_REPRESENTATION(#7655,#7732);
#7655=PRODUCT_DEFINITION_SHAPE('',$,#7762);
#7732=SHAPE_REPRESENTATION('',(#4393),#7592);
#7749=PRODUCT_DEFINITION_CONTEXT('part definition',#7838,'design');
#7762=PRODUCT_DEFINITION('Hex Nut - M8','Hex Nut - M8',#7791,#7749);
#7791=PRODUCT_DEFINITION_FORMATION('',$,#7852);
#7838=APPLICATION_CONTEXT(
'Core Data for Automotive Mechanical Design Process');
#7839=PRODUCT_CONTEXT('part definition',#7838,'mechanical');
#7852=PRODUCT('Hex Nut - M8','Hex Nut - M8','Hex Nut - M8',(#7839));
#7932=COLOUR_RGB('Black',0.12,0.14,0.17);
#7933=FILL_AREA_STYLE_COLOUR('',#7932);
#7934=FILL_AREA_STYLE('',(#7933));
#7935=SURFACE_STYLE_FILL_AREA(#7934);
#7936=SURFACE_SIDE_STYLE('',(#7935));
#7937=SURFACE_STYLE_USAGE(.BOTH.,#7936);
#7938=PRESENTATION_STYLE_ASSIGNMENT((#7937));
ENDSEC;
END-ISO-10303-21;
